ISO-10303-21;
HEADER;
/* Generated by software containing ST-Developer
 * from STEP Tools, Inc. (www.steptools.com) 
 */

FILE_DESCRIPTION(
/* description */ (''),
/* implementation_level */ '2;1');

FILE_NAME(
/* name */ 'Locking_Ring.step',
/* time_stamp */ '2026-10-23T17:22:31+06:00',
/* author */ (''),
/* organization */ (''),
/* preprocessor_version */ 'ST-DEVELOPER v20.2',
/* originating_system */ 'Autodesk Translation Framework v15.15.0.0',
/* authorisation */ '');

FILE_SCHEMA (('AUTOMOTIVE_DESIGN { 1 0 10303 214 3 1 1 }'));
ENDSEC;

DATA;
#10=MECHANICAL_DESIGN_GEOMETRIC_PRESENTATION_REPRESENTATION('',(#78),#7315);
#53=(
BOUNDED_CURVE()
B_SPLINE_CURVE(2,(#5649,#5650,#5651),.UNSPECIFIED.,.F.,.F.)
B_SPLINE_CURVE_WITH_KNOTS((3,3),(0.34166803276061,0.426429000654806),
 .UNSPECIFIED.)
CURVE()
GEOMETRIC_REPRESENTATION_ITEM()
RATIONAL_B_SPLINE_CURVE((1.00724935954325,1.0045238899297,1.))
REPRESENTATION_ITEM('')
);
#54=(
BOUNDED_CURVE()
B_SPLINE_CURVE(2,(#5655,#5656,#5657),.UNSPECIFIED.,.F.,.F.)
B_SPLINE_CURVE_WITH_KNOTS((3,3),(0.,0.0847609678918292),.UNSPECIFIED.)
CURVE()
GEOMETRIC_REPRESENTATION_ITEM()
RATIONAL_B_SPLINE_CURVE((1.,1.00452388992958,1.0072493595431))
REPRESENTATION_ITEM('')
);
#55=(
BOUNDED_CURVE()
B_SPLINE_CURVE(2,(#5669,#5670,#5671),.UNSPECIFIED.,.F.,.F.)
B_SPLINE_CURVE_WITH_KNOTS((3,3),(0.,0.0847609678918293),.UNSPECIFIED.)
CURVE()
GEOMETRIC_REPRESENTATION_ITEM()
RATIONAL_B_SPLINE_CURVE((1.,1.00452388992958,1.0072493595431))
REPRESENTATION_ITEM('')
);
#56=(
BOUNDED_CURVE()
B_SPLINE_CURVE(2,(#5678,#5679,#5680),.UNSPECIFIED.,.F.,.F.)
B_SPLINE_CURVE_WITH_KNOTS((3,3),(0.34166803276061,0.426429000654806),
 .UNSPECIFIED.)
CURVE()
GEOMETRIC_REPRESENTATION_ITEM()
RATIONAL_B_SPLINE_CURVE((1.00724935954325,1.0045238899297,1.))
REPRESENTATION_ITEM('')
);
#58=SHAPE_REPRESENTATION_RELATIONSHIP('SRR','None',#7354,#68);
#68=ADVANCED_BREP_SHAPE_REPRESENTATION('',(#88),#7306);
#78=STYLED_ITEM('',(#7438),#88);
#88=MANIFOLD_SOLID_BREP('Locking_Ring',#3215);
#99=CONICAL_SURFACE('',#3453,5.97286361298787,0.785398163397449);
#100=CONICAL_SURFACE('',#3459,5.97286361298787,0.785398163397449);
#283=LINE('',#5661,#443);
#284=LINE('',#5664,#444);
#285=LINE('',#5667,#445);
#286=LINE('',#5673,#446);
#287=LINE('',#5674,#447);
#288=LINE('',#5684,#448);
#289=LINE('',#5687,#449);
#290=LINE('',#5688,#450);
#443=VECTOR('',#4022,10.);
#444=VECTOR('',#4025,10.);
#445=VECTOR('',#4028,10.);
#446=VECTOR('',#4029,10.);
#447=VECTOR('',#4030,10.);
#448=VECTOR('',#4039,10.);
#449=VECTOR('',#4042,10.);
#450=VECTOR('',#4043,10.);
#601=CYLINDRICAL_SURFACE('',#3462,6.22286361298787);
#602=CYLINDRICAL_SURFACE('',#3464,4.72286361298787);
#703=PLANE('',#3456);
#704=PLANE('',#3458);
#705=PLANE('',#3463);
#706=PLANE('',#3466);
#786=FACE_OUTER_BOUND('',#969,.T.);
#787=FACE_OUTER_BOUND('',#970,.T.);
#788=FACE_OUTER_BOUND('',#971,.T.);
#789=FACE_OUTER_BOUND('',#972,.T.);
#790=FACE_OUTER_BOUND('',#973,.T.);
#791=FACE_OUTER_BOUND('',#974,.T.);
#792=FACE_OUTER_BOUND('',#975,.T.);
#793=FACE_OUTER_BOUND('',#976,.T.);
#969=EDGE_LOOP('',(#2406,#2407,#2408,#2409));
#970=EDGE_LOOP('',(#2410,#2411,#2412,#2413));
#971=EDGE_LOOP('',(#2414,#2415,#2416,#2417,#2418,#2419));
#972=EDGE_LOOP('',(#2420,#2421,#2422,#2423));
#973=EDGE_LOOP('',(#2424,#2425,#2426,#2427));
#974=EDGE_LOOP('',(#2428,#2429,#2430,#2431,#2432,#2433));
#975=EDGE_LOOP('',(#2434,#2435,#2436,#2437));
#976=EDGE_LOOP('',(#2438,#2439,#2440,#2441));
#1160=CIRCLE('',#3454,5.72286361298787);
#1161=CIRCLE('',#3455,6.22286361298787);
#1162=CIRCLE('',#3457,4.72286361298787);
#1163=CIRCLE('',#3460,5.72286361298787);
#1164=CIRCLE('',#3461,6.22286361298787);
#1165=CIRCLE('',#3465,4.72286361298787);
#1397=VERTEX_POINT('',#5647);
#1398=VERTEX_POINT('',#5648);
#1399=VERTEX_POINT('',#5652);
#1400=VERTEX_POINT('',#5654);
#1401=VERTEX_POINT('',#5660);
#1402=VERTEX_POINT('',#5662);
#1403=VERTEX_POINT('',#5666);
#1404=VERTEX_POINT('',#5668);
#1405=VERTEX_POINT('',#5672);
#1406=VERTEX_POINT('',#5676);
#1407=VERTEX_POINT('',#5677);
#1408=VERTEX_POINT('',#5686);
#1769=EDGE_CURVE('',#1397,#1398,#53,.T.);
#1770=EDGE_CURVE('',#1398,#1399,#1160,.T.);
#1771=EDGE_CURVE('',#1399,#1400,#54,.T.);
#1772=EDGE_CURVE('',#1400,#1397,#1161,.T.);
#1773=EDGE_CURVE('',#1398,#1401,#283,.T.);
#1774=EDGE_CURVE('',#1401,#1402,#1162,.T.);
#1775=EDGE_CURVE('',#1402,#1399,#284,.T.);
#1776=EDGE_CURVE('',#1403,#1397,#285,.T.);
#1777=EDGE_CURVE('',#1404,#1403,#55,.T.);
#1778=EDGE_CURVE('',#1404,#1405,#286,.T.);
#1779=EDGE_CURVE('',#1405,#1401,#287,.T.);
#1780=EDGE_CURVE('',#1406,#1407,#56,.T.);
#1781=EDGE_CURVE('',#1407,#1404,#1163,.T.);
#1782=EDGE_CURVE('',#1403,#1406,#1164,.T.);
#1783=EDGE_CURVE('',#1406,#1400,#288,.F.);
#1784=EDGE_CURVE('',#1408,#1402,#289,.T.);
#1785=EDGE_CURVE('',#1408,#1407,#290,.T.);
#1786=EDGE_CURVE('',#1405,#1408,#1165,.T.);
#2406=ORIENTED_EDGE('',*,*,#1769,.T.);
#2407=ORIENTED_EDGE('',*,*,#1770,.T.);
#2408=ORIENTED_EDGE('',*,*,#1771,.T.);
#2409=ORIENTED_EDGE('',*,*,#1772,.T.);
#2410=ORIENTED_EDGE('',*,*,#1770,.F.);
#2411=ORIENTED_EDGE('',*,*,#1773,.T.);
#2412=ORIENTED_EDGE('',*,*,#1774,.T.);
#2413=ORIENTED_EDGE('',*,*,#1775,.T.);
#2414=ORIENTED_EDGE('',*,*,#1769,.F.);
#2415=ORIENTED_EDGE('',*,*,#1776,.F.);
#2416=ORIENTED_EDGE('',*,*,#1777,.F.);
#2417=ORIENTED_EDGE('',*,*,#1778,.T.);
#2418=ORIENTED_EDGE('',*,*,#1779,.T.);
#2419=ORIENTED_EDGE('',*,*,#1773,.F.);
#2420=ORIENTED_EDGE('',*,*,#1780,.T.);
#2421=ORIENTED_EDGE('',*,*,#1781,.T.);
#2422=ORIENTED_EDGE('',*,*,#1777,.T.);
#2423=ORIENTED_EDGE('',*,*,#1782,.T.);
#2424=ORIENTED_EDGE('',*,*,#1772,.F.);
#2425=ORIENTED_EDGE('',*,*,#1783,.F.);
#2426=ORIENTED_EDGE('',*,*,#1782,.F.);
#2427=ORIENTED_EDGE('',*,*,#1776,.T.);
#2428=ORIENTED_EDGE('',*,*,#1771,.F.);
#2429=ORIENTED_EDGE('',*,*,#1775,.F.);
#2430=ORIENTED_EDGE('',*,*,#1784,.F.);
#2431=ORIENTED_EDGE('',*,*,#1785,.T.);
#2432=ORIENTED_EDGE('',*,*,#1780,.F.);
#2433=ORIENTED_EDGE('',*,*,#1783,.T.);
#2434=ORIENTED_EDGE('',*,*,#1786,.T.);
#2435=ORIENTED_EDGE('',*,*,#1784,.T.);
#2436=ORIENTED_EDGE('',*,*,#1774,.F.);
#2437=ORIENTED_EDGE('',*,*,#1779,.F.);
#2438=ORIENTED_EDGE('',*,*,#1781,.F.);
#2439=ORIENTED_EDGE('',*,*,#1785,.F.);
#2440=ORIENTED_EDGE('',*,*,#1786,.F.);
#2441=ORIENTED_EDGE('',*,*,#1778,.F.);
#3090=ADVANCED_FACE('',(#786),#99,.T.);
#3091=ADVANCED_FACE('',(#787),#703,.F.);
#3092=ADVANCED_FACE('',(#788),#704,.T.);
#3093=ADVANCED_FACE('',(#789),#100,.T.);
#3094=ADVANCED_FACE('',(#790),#601,.T.);
#3095=ADVANCED_FACE('',(#791),#705,.T.);
#3096=ADVANCED_FACE('',(#792),#602,.F.);
#3097=ADVANCED_FACE('',(#793),#706,.T.);
#3215=CLOSED_SHELL('',(#3090,#3091,#3092,#3093,#3094,#3095,#3096,#3097));
#3452=AXIS2_PLACEMENT_3D('',#5645,#4012,#4013);
#3453=AXIS2_PLACEMENT_3D('',#5646,#4014,#4015);
#3454=AXIS2_PLACEMENT_3D('',#5653,#4016,#4017);
#3455=AXIS2_PLACEMENT_3D('',#5658,#4018,#4019);
#3456=AXIS2_PLACEMENT_3D('',#5659,#4020,#4021);
#3457=AXIS2_PLACEMENT_3D('',#5663,#4023,#4024);
#3458=AXIS2_PLACEMENT_3D('',#5665,#4026,#4027);
#3459=AXIS2_PLACEMENT_3D('',#5675,#4031,#4032);
#3460=AXIS2_PLACEMENT_3D('',#5681,#4033,#4034);
#3461=AXIS2_PLACEMENT_3D('',#5682,#4035,#4036);
#3462=AXIS2_PLACEMENT_3D('',#5683,#4037,#4038);
#3463=AXIS2_PLACEMENT_3D('',#5685,#4040,#4041);
#3464=AXIS2_PLACEMENT_3D('',#5689,#4044,#4045);
#3465=AXIS2_PLACEMENT_3D('',#5690,#4046,#4047);
#3466=AXIS2_PLACEMENT_3D('',#5691,#4048,#4049);
#4012=DIRECTION('axis',(0.,0.,1.));
#4013=DIRECTION('refdir',(1.,0.,0.));
#4014=DIRECTION('center_axis',(-1.,0.,0.));
#4015=DIRECTION('ref_axis',(0.,1.83697019872103E-16,-1.));
#4016=DIRECTION('center_axis',(-1.,0.,0.));
#4017=DIRECTION('ref_axis',(0.,-1.,0.));
#4018=DIRECTION('center_axis',(1.,0.,0.));
#4019=DIRECTION('ref_axis',(0.,-1.,0.));
#4020=DIRECTION('center_axis',(-1.,0.,0.));
#4021=DIRECTION('ref_axis',(0.,-1.,0.));
#4022=DIRECTION('',(0.,0.,-1.));
#4023=DIRECTION('center_axis',(-1.,0.,0.));
#4024=DIRECTION('ref_axis',(0.,-1.,0.));
#4025=DIRECTION('',(0.,0.,1.));
#4026=DIRECTION('center_axis',(0.,-1.,0.));
#4027=DIRECTION('ref_axis',(0.,0.,-1.));
#4028=DIRECTION('',(1.,0.,0.));
#4029=DIRECTION('',(0.,0.,-1.));
#4030=DIRECTION('',(1.,0.,0.));
#4031=DIRECTION('center_axis',(1.,0.,0.));
#4032=DIRECTION('ref_axis',(0.,-6.12323399573677E-17,-1.));
#4033=DIRECTION('center_axis',(1.,0.,0.));
#4034=DIRECTION('ref_axis',(0.,-1.,0.));
#4035=DIRECTION('center_axis',(-1.,0.,0.));
#4036=DIRECTION('ref_axis',(0.,-1.,0.));
#4037=DIRECTION('center_axis',(1.,0.,0.));
#4038=DIRECTION('ref_axis',(0.,-2.83276944882399E-16,-1.));
#4039=DIRECTION('',(-1.,0.,0.));
#4040=DIRECTION('center_axis',(0.,1.,0.));
#4041=DIRECTION('ref_axis',(0.,0.,1.));
#4042=DIRECTION('',(1.,0.,0.));
#4043=DIRECTION('',(0.,0.,1.));
#4044=DIRECTION('center_axis',(1.,0.,0.));
#4045=DIRECTION('ref_axis',(0.,-6.12323399573677E-17,-1.));
#4046=DIRECTION('center_axis',(-1.,0.,0.));
#4047=DIRECTION('ref_axis',(0.,-1.,0.));
#4048=DIRECTION('center_axis',(-1.,0.,0.));
#4049=DIRECTION('ref_axis',(0.,-1.,0.));
#5645=CARTESIAN_POINT('',(0.,0.,0.));
#5646=CARTESIAN_POINT('Origin',(4.25,0.,0.));
#5647=CARTESIAN_POINT('',(4.,1.,6.1419892173341));
#5648=CARTESIAN_POINT('',(4.5,1.,5.63481747112189));
#5649=CARTESIAN_POINT('Ctrl Pts',(4.,1.,6.1419892173341));
#5650=CARTESIAN_POINT('Ctrl Pts',(4.26076632571102,1.,5.87778926153153));
#5651=CARTESIAN_POINT('Ctrl Pts',(4.5,1.,5.63481747112189));
#5652=CARTESIAN_POINT('',(4.5,-1.,5.63481747112189));
#5653=CARTESIAN_POINT('Origin',(4.5,0.,0.));
#5654=CARTESIAN_POINT('',(4.,-1.,6.1419892173341));
#5655=CARTESIAN_POINT('Ctrl Pts',(4.5,-1.,5.63481747112189));
#5656=CARTESIAN_POINT('Ctrl Pts',(4.26076632570315,-1.,5.87778926153949));
#5657=CARTESIAN_POINT('Ctrl Pts',(4.,-1.,6.1419892173341));
#5658=CARTESIAN_POINT('Origin',(4.,0.,0.));
#5659=CARTESIAN_POINT('Origin',(4.5,0.,-0.0373945338826487));
#5660=CARTESIAN_POINT('',(4.5,1.,4.6157817005232));
#5661=CARTESIAN_POINT('',(4.5,1.,9.13904432441494));
#5662=CARTESIAN_POINT('',(4.5,-1.,4.61578170052319));
#5663=CARTESIAN_POINT('Origin',(4.5,0.,0.));
#5664=CARTESIAN_POINT('',(4.5,-1.,-9.13904432441494));
#5665=CARTESIAN_POINT('Origin',(1.5,1.,6.64807454522257));
#5666=CARTESIAN_POINT('',(2.,1.,6.1419892173341));
#5667=CARTESIAN_POINT('',(1.5,1.,6.1419892173341));
#5668=CARTESIAN_POINT('',(1.5,1.,5.63481747112189));
#5669=CARTESIAN_POINT('Ctrl Pts',(1.5,1.,5.63481747112189));
#5670=CARTESIAN_POINT('Ctrl Pts',(1.73923367429685,1.,5.87778926153949));
#5671=CARTESIAN_POINT('Ctrl Pts',(2.,1.,6.1419892173341));
#5672=CARTESIAN_POINT('',(1.5,1.,4.6157817005232));
#5673=CARTESIAN_POINT('',(1.5,1.,9.13904432441494));
#5674=CARTESIAN_POINT('',(1.5,1.,4.6157817005232));
#5675=CARTESIAN_POINT('Origin',(1.75,0.,0.));
#5676=CARTESIAN_POINT('',(2.,-1.,6.1419892173341));
#5677=CARTESIAN_POINT('',(1.5,-1.,5.63481747112189));
#5678=CARTESIAN_POINT('Ctrl Pts',(2.,-1.,6.1419892173341));
#5679=CARTESIAN_POINT('Ctrl Pts',(1.73923367428898,-1.,5.87778926153153));
#5680=CARTESIAN_POINT('Ctrl Pts',(1.5,-1.,5.63481747112189));
#5681=CARTESIAN_POINT('Origin',(1.5,0.,0.));
#5682=CARTESIAN_POINT('Origin',(2.,0.,0.));
#5683=CARTESIAN_POINT('Origin',(1.5,0.,0.));
#5684=CARTESIAN_POINT('',(1.5,-1.,6.1419892173341));
#5685=CARTESIAN_POINT('Origin',(1.5,-1.,4.61578170052319));
#5686=CARTESIAN_POINT('',(1.5,-1.,4.61578170052319));
#5687=CARTESIAN_POINT('',(1.5,-1.,4.61578170052319));
#5688=CARTESIAN_POINT('',(1.5,-1.,-9.13904432441494));
#5689=CARTESIAN_POINT('Origin',(1.5,0.,0.));
#5690=CARTESIAN_POINT('Origin',(1.5,0.,0.));
#5691=CARTESIAN_POINT('Origin',(1.5,0.,-0.0373945338826487));
#7294=UNCERTAINTY_MEASURE_WITH_UNIT(LENGTH_MEASURE(0.01),#7316,
'DISTANCE_ACCURACY_VALUE',
'Maximum model space distance between geometric entities at asserted c
onnectivities');
#7303=UNCERTAINTY_MEASURE_WITH_UNIT(LENGTH_MEASURE(0.01),#7316,
'DISTANCE_ACCURACY_VALUE',
'Maximum model space distance between geometric entities at asserted c
onnectivities');
#7306=(
GEOMETRIC_REPRESENTATION_CONTEXT(3)
GLOBAL_UNCERTAINTY_ASSIGNED_CONTEXT((#7294))
GLOBAL_UNIT_ASSIGNED_CONTEXT((#7316,#7318,#7319))
REPRESENTATION_CONTEXT('','3D')
);
#7315=(
GEOMETRIC_REPRESENTATION_CONTEXT(3)
GLOBAL_UNCERTAINTY_ASSIGNED_CONTEXT((#7303))
GLOBAL_UNIT_ASSIGNED_CONTEXT((#7316,#7318,#7319))
REPRESENTATION_CONTEXT('','3D')
);
#7316=(
LENGTH_UNIT()
NAMED_UNIT(*)
SI_UNIT(.MILLI.,.METRE.)
);
#7318=(
NAMED_UNIT(*)
PLANE_ANGLE_UNIT()
SI_UNIT($,.RADIAN.)
);
#7319=(
NAMED_UNIT(*)
SI_UNIT($,.STERADIAN.)
SOLID_ANGLE_UNIT()
);
#7322=SHAPE_DEFINITION_REPRESENTATION(#7333,#7354);
#7333=PRODUCT_DEFINITION_SHAPE('',$,#7366);
#7354=SHAPE_REPRESENTATION('',(#3452),#7306);
#7363=PRODUCT_DEFINITION_CONTEXT('part definition',#7398,'design');
#7366=PRODUCT_DEFINITION('Locking_Ring','Locking_Ring',#7377,#7363);
#7377=PRODUCT_DEFINITION_FORMATION('',$,#7402);
#7398=APPLICATION_CONTEXT(
'Core Data for Automotive Mechanical Design Process');
#7399=PRODUCT_CONTEXT('part definition',#7398,'mechanical');
#7402=PRODUCT('Locking_Ring','Locking_Ring',$,(#7399));
#7432=COLOUR_RGB('Sky Blue',0.24,0.69,0.87);
#7433=FILL_AREA_STYLE_COLOUR('',#7432);
#7434=FILL_AREA_STYLE('',(#7433));
#7435=SURFACE_STYLE_FILL_AREA(#7434);
#7436=SURFACE_SIDE_STYLE('',(#7435));
#7437=SURFACE_STYLE_USAGE(.BOTH.,#7436);
#7438=PRESENTATION_STYLE_ASSIGNMENT((#7437));
ENDSEC;
END-ISO-10303-21;
